ISO-10303-21;
HEADER;
/* Generated by software containing ST-Developer
 * from STEP Tools, Inc. (www.steptools.com) 
 */

FILE_DESCRIPTION(
/* description */ ('PAT-091'),
/* implementation_level */ '2;1');

FILE_NAME(
/* name */ 'M4 low-profile retaining screw (11).step',
/* time_stamp */ '2026-10-27T15:34:44-07:00',
/* author */ (''),
/* organization */ (''),
/* preprocessor_version */ 'ST-DEVELOPER v20.2',
/* originating_system */ 'Autodesk Translation Framework v15.17.0.0',
/* authorisation */ '');

FILE_SCHEMA (('AUTOMOTIVE_DESIGN { 1 0 10303 214 3 1 1 }'));
ENDSEC;

DATA;
#10=MECHANICAL_DESIGN_GEOMETRIC_PRESENTATION_REPRESENTATION('',(#1064),#25100);
#844=SHAPE_REPRESENTATION_RELATIONSHIP('SRR','None',#25611,#954);
#954=ADVANCED_BREP_SHAPE_REPRESENTATION('',(#1185),#25081);
#1064=STYLED_ITEM('',(#26198),#1185);
#1185=MANIFOLD_SOLID_BREP('Body1',#13344);
#1602=FACE_BOUND('',#3948,.T.);
#2007=PLANE('',#16062);
#2008=PLANE('',#16067);
#2009=PLANE('',#16070);
#2742=FACE_OUTER_BOUND('',#3947,.T.);
#2743=FACE_OUTER_BOUND('',#3949,.T.);
#2744=FACE_OUTER_BOUND('',#3950,.T.);
#2745=FACE_OUTER_BOUND('',#3951,.T.);
#2746=FACE_OUTER_BOUND('',#3952,.T.);
#3947=EDGE_LOOP('',(#11612));
#3948=EDGE_LOOP('',(#11613));
#3949=EDGE_LOOP('',(#11614,#11615,#11616,#11617));
#3950=EDGE_LOOP('',(#11618));
#3951=EDGE_LOOP('',(#11619,#11620,#11621,#11622));
#3952=EDGE_LOOP('',(#11623));
#4818=LINE('',#24084,#5558);
#4819=LINE('',#24090,#5559);
#5558=VECTOR('',#20124,0.350000000000001);
#5559=VECTOR('',#20133,0.199999999999999);
#6226=CIRCLE('',#16063,0.350000000000001);
#6227=CIRCLE('',#16064,0.199999999999999);
#6228=CIRCLE('',#16066,0.350000000000001);
#6229=CIRCLE('',#16069,0.199999999999999);
#7259=VERTEX_POINT('',#24078);
#7260=VERTEX_POINT('',#24080);
#7261=VERTEX_POINT('',#24083);
#7262=VERTEX_POINT('',#24088);
#8741=EDGE_CURVE('',#7259,#7259,#6226,.T.);
#8742=EDGE_CURVE('',#7260,#7260,#6227,.T.);
#8743=EDGE_CURVE('',#7259,#7261,#4818,.T.);
#8744=EDGE_CURVE('',#7261,#7261,#6228,.T.);
#8745=EDGE_CURVE('',#7262,#7262,#6229,.T.);
#8746=EDGE_CURVE('',#7262,#7260,#4819,.T.);
#11612=ORIENTED_EDGE('',*,*,#8741,.T.);
#11613=ORIENTED_EDGE('',*,*,#8742,.F.);
#11614=ORIENTED_EDGE('',*,*,#8741,.F.);
#11615=ORIENTED_EDGE('',*,*,#8743,.T.);
#11616=ORIENTED_EDGE('',*,*,#8744,.T.);
#11617=ORIENTED_EDGE('',*,*,#8743,.F.);
#11618=ORIENTED_EDGE('',*,*,#8744,.F.);
#11619=ORIENTED_EDGE('',*,*,#8745,.F.);
#11620=ORIENTED_EDGE('',*,*,#8746,.T.);
#11621=ORIENTED_EDGE('',*,*,#8742,.T.);
#11622=ORIENTED_EDGE('',*,*,#8746,.F.);
#11623=ORIENTED_EDGE('',*,*,#8745,.T.);
#12374=CYLINDRICAL_SURFACE('',#16065,0.350000000000001);
#12375=CYLINDRICAL_SURFACE('',#16068,0.199999999999999);
#13109=ADVANCED_FACE('',(#2742,#1602),#2007,.T.);
#13110=ADVANCED_FACE('',(#2743),#12374,.T.);
#13111=ADVANCED_FACE('',(#2744),#2008,.F.);
#13112=ADVANCED_FACE('',(#2745),#12375,.T.);
#13113=ADVANCED_FACE('',(#2746),#2009,.T.);
#13344=CLOSED_SHELL('',(#13109,#13110,#13111,#13112,#13113));
#16061=AXIS2_PLACEMENT_3D('',#24076,#20114,#20115);
#16062=AXIS2_PLACEMENT_3D('',#24077,#20116,#20117);
#16063=AXIS2_PLACEMENT_3D('',#24079,#20118,#20119);
#16064=AXIS2_PLACEMENT_3D('',#24081,#20120,#20121);
#16065=AXIS2_PLACEMENT_3D('',#24082,#20122,#20123);
#16066=AXIS2_PLACEMENT_3D('',#24085,#20125,#20126);
#16067=AXIS2_PLACEMENT_3D('',#24086,#20127,#20128);
#16068=AXIS2_PLACEMENT_3D('',#24087,#20129,#20130);
#16069=AXIS2_PLACEMENT_3D('',#24089,#20131,#20132);
#16070=AXIS2_PLACEMENT_3D('',#24091,#20134,#20135);
#20114=DIRECTION('axis',(0.,0.,1.));
#20115=DIRECTION('refdir',(1.,0.,0.));
#20116=DIRECTION('center_axis',(0.,1.,0.));
#20117=DIRECTION('ref_axis',(1.,0.,0.));
#20118=DIRECTION('center_axis',(0.,1.,0.));
#20119=DIRECTION('ref_axis',(1.,0.,0.));
#20120=DIRECTION('center_axis',(0.,1.,0.));
#20121=DIRECTION('ref_axis',(1.,0.,0.));
#20122=DIRECTION('center_axis',(0.,1.,0.));
#20123=DIRECTION('ref_axis',(1.,0.,0.));
#20124=DIRECTION('',(0.,-1.,0.));
#20125=DIRECTION('center_axis',(0.,1.,0.));
#20126=DIRECTION('ref_axis',(1.,0.,0.));
#20127=DIRECTION('center_axis',(0.,1.,0.));
#20128=DIRECTION('ref_axis',(1.,0.,0.));
#20129=DIRECTION('center_axis',(0.,1.,0.));
#20130=DIRECTION('ref_axis',(1.,0.,0.));
#20131=DIRECTION('center_axis',(0.,1.,0.));
#20132=DIRECTION('ref_axis',(1.,0.,0.));
#20133=DIRECTION('',(0.,-1.,0.));
#20134=DIRECTION('center_axis',(0.,1.,0.));
#20135=DIRECTION('ref_axis',(1.,0.,0.));
#24076=CARTESIAN_POINT('',(0.,0.,0.));
#24077=CARTESIAN_POINT('Origin',(20.6730642762322,6.7,6.69185245480489));
#24078=CARTESIAN_POINT('',(20.3230642762322,6.7,6.69185245480489));
#24079=CARTESIAN_POINT('Origin',(20.6730642762322,6.7,6.69185245480489));
#24080=CARTESIAN_POINT('',(20.4730642762322,6.7,6.69185245480489));
#24081=CARTESIAN_POINT('Origin',(20.6730642762322,6.7,6.69185245480489));
#24082=CARTESIAN_POINT('Origin',(20.6730642762322,6.6,6.69185245480489));
#24083=CARTESIAN_POINT('',(20.3230642762322,6.6,6.69185245480489));
#24084=CARTESIAN_POINT('',(20.3230642762322,6.6,6.69185245480489));
#24085=CARTESIAN_POINT('Origin',(20.6730642762322,6.6,6.69185245480489));
#24086=CARTESIAN_POINT('Origin',(20.6730642762322,6.6,6.69185245480489));
#24087=CARTESIAN_POINT('Origin',(20.6730642762322,6.7,6.69185245480489));
#24088=CARTESIAN_POINT('',(20.4730642762322,7.4,6.69185245480489));
#24089=CARTESIAN_POINT('Origin',(20.6730642762322,7.4,6.69185245480489));
#24090=CARTESIAN_POINT('',(20.4730642762322,6.7,6.69185245480489));
#24091=CARTESIAN_POINT('Origin',(20.6730642762322,7.4,6.69185245480489));
#24960=UNCERTAINTY_MEASURE_WITH_UNIT(LENGTH_MEASURE(0.001),#25101,
'DISTANCE_ACCURACY_VALUE',
'Maximum model space distance between geometric entities at asserted c
onnectivities');
#24979=UNCERTAINTY_MEASURE_WITH_UNIT(LENGTH_MEASURE(0.001),#25101,
'DISTANCE_ACCURACY_VALUE',
'Maximum model space distance between geometric entities at asserted c
onnectivities');
#25081=(
GEOMETRIC_REPRESENTATION_CONTEXT(3)
GLOBAL_UNCERTAINTY_ASSIGNED_CONTEXT((#24960))
GLOBAL_UNIT_ASSIGNED_CONTEXT((#25101,#25103,#25104))
REPRESENTATION_CONTEXT('','3D')
);
#25100=(
GEOMETRIC_REPRESENTATION_CONTEXT(3)
GLOBAL_UNCERTAINTY_ASSIGNED_CONTEXT((#24979))
GLOBAL_UNIT_ASSIGNED_CONTEXT((#25101,#25103,#25104))
REPRESENTATION_CONTEXT('','3D')
);
#25101=(
LENGTH_UNIT()
NAMED_UNIT(*)
SI_UNIT(.CENTI.,.METRE.)
);
#25103=(
NAMED_UNIT(*)
PLANE_ANGLE_UNIT()
SI_UNIT($,.RADIAN.)
);
#25104=(
NAMED_UNIT(*)
SI_UNIT($,.STERADIAN.)
SOLID_ANGLE_UNIT()
);
#25206=SHAPE_DEFINITION_REPRESENTATION(#25400,#25611);
#25400=PRODUCT_DEFINITION_SHAPE('',$,#25732);
#25611=SHAPE_REPRESENTATION('',(#16061),#25081);
#25630=PRODUCT_DEFINITION_CONTEXT('part definition',#25992,'design');
#25732=PRODUCT_DEFINITION('M4 low-profile retaining screw (11)',
'M4 low-profile retaining screw (11)',#25852,#25630);
#25852=PRODUCT_DEFINITION_FORMATION('',$,#26095);
#25992=APPLICATION_CONTEXT(
'Core Data for Automotive Mechanical Design Process');
#25993=PRODUCT_CONTEXT('part definition',#25992,'mechanical');
#26095=PRODUCT('M4 low-profile retaining screw (11)',
'M4 low-profile retaining screw (11)','M4 low-profile retaining screw (11)',
(#25993));
#26192=COLOUR_RGB('Black',0.12,0.14,0.17);
#26193=FILL_AREA_STYLE_COLOUR('',#26192);
#26194=FILL_AREA_STYLE('',(#26193));
#26195=SURFACE_STYLE_FILL_AREA(#26194);
#26196=SURFACE_SIDE_STYLE('',(#26195));
#26197=SURFACE_STYLE_USAGE(.BOTH.,#26196);
#26198=PRESENTATION_STYLE_ASSIGNMENT((#26197));
ENDSEC;
END-ISO-10303-21;
